ISO-10303-21;
HEADER;
/* Generated by software containing ST-Developer
 * from STEP Tools, Inc. (www.steptools.com) 
 */

FILE_DESCRIPTION(
/* description */ ('PAT-091'),
/* implementation_level */ '2;1');

FILE_NAME(
/* name */ 'Plain pivot bush (2).step',
/* time_stamp */ '2026-10-27T15:34:44-07:00',
/* author */ (''),
/* organization */ (''),
/* preprocessor_version */ 'ST-DEVELOPER v20.2',
/* originating_system */ 'Autodesk Translation Framework v15.17.0.0',
/* authorisation */ '');

FILE_SCHEMA (('AUTOMOTIVE_DESIGN { 1 0 10303 214 3 1 1 }'));
ENDSEC;

DATA;
#10=MECHANICAL_DESIGN_GEOMETRIC_PRESENTATION_REPRESENTATION('',(#1030),#25100);
#810=SHAPE_REPRESENTATION_RELATIONSHIP('SRR','None',#25576,#920);
#920=ADVANCED_BREP_SHAPE_REPRESENTATION('',(#1152),#25046);
#1030=STYLED_ITEM('',(#26177),#1152);
#1152=MANIFOLD_SOLID_BREP('Body1',#13309);
#1494=FACE_BOUND('',#3632,.T.);
#1495=FACE_BOUND('',#3634,.T.);
#1905=PLANE('',#15539);
#1906=PLANE('',#15540);
#2532=FACE_OUTER_BOUND('',#3629,.T.);
#2533=FACE_OUTER_BOUND('',#3630,.T.);
#2534=FACE_OUTER_BOUND('',#3631,.T.);
#2535=FACE_OUTER_BOUND('',#3633,.T.);
#3629=EDGE_LOOP('',(#10864,#10865,#10866,#10867));
#3630=EDGE_LOOP('',(#10868,#10869,#10870,#10871));
#3631=EDGE_LOOP('',(#10872));
#3632=EDGE_LOOP('',(#10873));
#3633=EDGE_LOOP('',(#10874));
#3634=EDGE_LOOP('',(#10875));
#4656=LINE('',#23142,#5396);
#4657=LINE('',#23148,#5397);
#5396=VECTOR('',#18900,0.605);
#5397=VECTOR('',#18907,1.);
#6014=CIRCLE('',#15534,0.605);
#6015=CIRCLE('',#15535,0.605);
#6016=CIRCLE('',#15537,1.);
#6017=CIRCLE('',#15538,1.);
#7011=VERTEX_POINT('',#23139);
#7012=VERTEX_POINT('',#23141);
#7013=VERTEX_POINT('',#23145);
#7014=VERTEX_POINT('',#23147);
#8367=EDGE_CURVE('',#7011,#7011,#6014,.T.);
#8368=EDGE_CURVE('',#7011,#7012,#4656,.T.);
#8369=EDGE_CURVE('',#7012,#7012,#6015,.T.);
#8370=EDGE_CURVE('',#7013,#7013,#6016,.T.);
#8371=EDGE_CURVE('',#7013,#7014,#4657,.T.);
#8372=EDGE_CURVE('',#7014,#7014,#6017,.T.);
#10864=ORIENTED_EDGE('',*,*,#8367,.F.);
#10865=ORIENTED_EDGE('',*,*,#8368,.T.);
#10866=ORIENTED_EDGE('',*,*,#8369,.T.);
#10867=ORIENTED_EDGE('',*,*,#8368,.F.);
#10868=ORIENTED_EDGE('',*,*,#8370,.F.);
#10869=ORIENTED_EDGE('',*,*,#8371,.T.);
#10870=ORIENTED_EDGE('',*,*,#8372,.T.);
#10871=ORIENTED_EDGE('',*,*,#8371,.F.);
#10872=ORIENTED_EDGE('',*,*,#8370,.T.);
#10873=ORIENTED_EDGE('',*,*,#8367,.T.);
#10874=ORIENTED_EDGE('',*,*,#8372,.F.);
#10875=ORIENTED_EDGE('',*,*,#8369,.F.);
#12270=CYLINDRICAL_SURFACE('',#15533,0.605);
#12271=CYLINDRICAL_SURFACE('',#15536,1.);
#12899=ADVANCED_FACE('',(#2532),#12270,.F.);
#12900=ADVANCED_FACE('',(#2533),#12271,.T.);
#12901=ADVANCED_FACE('',(#2534,#1494),#1905,.T.);
#12902=ADVANCED_FACE('',(#2535,#1495),#1906,.F.);
#13309=CLOSED_SHELL('',(#12899,#12900,#12901,#12902));
#15532=AXIS2_PLACEMENT_3D('',#23137,#18894,#18895);
#15533=AXIS2_PLACEMENT_3D('',#23138,#18896,#18897);
#15534=AXIS2_PLACEMENT_3D('',#23140,#18898,#18899);
#15535=AXIS2_PLACEMENT_3D('',#23143,#18901,#18902);
#15536=AXIS2_PLACEMENT_3D('',#23144,#18903,#18904);
#15537=AXIS2_PLACEMENT_3D('',#23146,#18905,#18906);
#15538=AXIS2_PLACEMENT_3D('',#23149,#18908,#18909);
#15539=AXIS2_PLACEMENT_3D('',#23150,#18910,#18911);
#15540=AXIS2_PLACEMENT_3D('',#23151,#18912,#18913);
#18894=DIRECTION('axis',(0.,0.,1.));
#18895=DIRECTION('refdir',(1.,0.,0.));
#18896=DIRECTION('center_axis',(0.,1.,0.));
#18897=DIRECTION('ref_axis',(1.,0.,0.));
#18898=DIRECTION('center_axis',(0.,-1.,0.));
#18899=DIRECTION('ref_axis',(1.,0.,0.));
#18900=DIRECTION('',(0.,-1.,0.));
#18901=DIRECTION('center_axis',(0.,-1.,0.));
#18902=DIRECTION('ref_axis',(1.,0.,0.));
#18903=DIRECTION('center_axis',(0.,1.,0.));
#18904=DIRECTION('ref_axis',(1.,0.,0.));
#18905=DIRECTION('center_axis',(0.,1.,0.));
#18906=DIRECTION('ref_axis',(1.,0.,0.));
#18907=DIRECTION('',(0.,-1.,0.));
#18908=DIRECTION('center_axis',(0.,1.,0.));
#18909=DIRECTION('ref_axis',(1.,0.,0.));
#18910=DIRECTION('center_axis',(0.,1.,0.));
#18911=DIRECTION('ref_axis',(1.,0.,0.));
#18912=DIRECTION('center_axis',(0.,1.,0.));
#18913=DIRECTION('ref_axis',(1.,0.,0.));
#23137=CARTESIAN_POINT('',(0.,0.,0.));
#23138=CARTESIAN_POINT('Origin',(19.3649167310371,-7.,8.));
#23139=CARTESIAN_POINT('',(18.7599167310371,-6.,8.));
#23140=CARTESIAN_POINT('Origin',(19.3649167310371,-6.,8.));
#23141=CARTESIAN_POINT('',(18.7599167310371,-7.,8.));
#23142=CARTESIAN_POINT('',(18.7599167310371,-7.,8.));
#23143=CARTESIAN_POINT('Origin',(19.3649167310371,-7.,8.));
#23144=CARTESIAN_POINT('Origin',(19.3649167310371,-7.,8.));
#23145=CARTESIAN_POINT('',(18.3649167310371,-6.,8.));
#23146=CARTESIAN_POINT('Origin',(19.3649167310371,-6.,8.));
#23147=CARTESIAN_POINT('',(18.3649167310371,-7.,8.));
#23148=CARTESIAN_POINT('',(18.3649167310371,-7.,8.));
#23149=CARTESIAN_POINT('Origin',(19.3649167310371,-7.,8.));
#23150=CARTESIAN_POINT('Origin',(19.3649167310371,-6.,8.));
#23151=CARTESIAN_POINT('Origin',(19.3649167310371,-7.,8.));
#24925=UNCERTAINTY_MEASURE_WITH_UNIT(LENGTH_MEASURE(0.001),#25101,
'DISTANCE_ACCURACY_VALUE',
'Maximum model space distance between geometric entities at asserted c
onnectivities');
#24979=UNCERTAINTY_MEASURE_WITH_UNIT(LENGTH_MEASURE(0.001),#25101,
'DISTANCE_ACCURACY_VALUE',
'Maximum model space distance between geometric entities at asserted c
onnectivities');
#25046=(
GEOMETRIC_REPRESENTATION_CONTEXT(3)
GLOBAL_UNCERTAINTY_ASSIGNED_CONTEXT((#24925))
GLOBAL_UNIT_ASSIGNED_CONTEXT((#25101,#25103,#25104))
REPRESENTATION_CONTEXT('','3D')
);
#25100=(
GEOMETRIC_REPRESENTATION_CONTEXT(3)
GLOBAL_UNCERTAINTY_ASSIGNED_CONTEXT((#24979))
GLOBAL_UNIT_ASSIGNED_CONTEXT((#25101,#25103,#25104))
REPRESENTATION_CONTEXT('','3D')
);
#25101=(
LENGTH_UNIT()
NAMED_UNIT(*)
SI_UNIT(.CENTI.,.METRE.)
);
#25103=(
NAMED_UNIT(*)
PLANE_ANGLE_UNIT()
SI_UNIT($,.RADIAN.)
);
#25104=(
NAMED_UNIT(*)
SI_UNIT($,.STERADIAN.)
SOLID_ANGLE_UNIT()
);
#25171=SHAPE_DEFINITION_REPRESENTATION(#25293,#25576);
#25293=PRODUCT_DEFINITION_SHAPE('',$,#25697);
#25576=SHAPE_REPRESENTATION('',(#15532),#25046);
#25630=PRODUCT_DEFINITION_CONTEXT('part definition',#25992,'design');
#25697=PRODUCT_DEFINITION('Plain pivot bush (2)','Plain pivot bush (2)',#25817,
#25630);
#25817=PRODUCT_DEFINITION_FORMATION('',$,#26060);
#25992=APPLICATION_CONTEXT(
'Core Data for Automotive Mechanical Design Process');
#25993=PRODUCT_CONTEXT('part definition',#25992,'mechanical');
#26060=PRODUCT('Plain pivot bush (2)','Plain pivot bush (2)',
'Plain pivot bush (2)',(#25993));
#26171=COLOUR_RGB('Light Blue',0.38,0.62,0.78);
#26172=FILL_AREA_STYLE_COLOUR('',#26171);
#26173=FILL_AREA_STYLE('',(#26172));
#26174=SURFACE_STYLE_FILL_AREA(#26173);
#26175=SURFACE_SIDE_STYLE('',(#26174));
#26176=SURFACE_STYLE_USAGE(.BOTH.,#26175);
#26177=PRESENTATION_STYLE_ASSIGNMENT((#26176));
ENDSEC;
END-ISO-10303-21;
